ISO-10303-21;
HEADER;
FILE_DESCRIPTION (('STEP AP214'),
    '1' );
FILE_NAME ('10. Bolt M10x25.step',
    '2026-10-09T08:13:37',
    ( '' ),
    ( '' ),
    'SwSTEP 2.0',
    'SolidWorks 2021',
    '' );
FILE_SCHEMA (( 'AUTOMOTIVE_DESIGN' ));
ENDSEC;

DATA;
#52=CARTESIAN_POINT ( 'NONE',  ( -5.603568002170371543, -8.294335516573692502, 0.9848892659495209756 ) ) ;
#184=CARTESIAN_POINT ( 'NONE',  ( 7.249999999999999112, 8.878689293818310074E-16, 0.7500000000000000000 ) ) ;
#204=EDGE_LOOP ( 'NONE', ( #41831, #44506, #36977, #5553, #63644 ) ) ;
#416=CARTESIAN_POINT ( 'NONE',  ( -7.566679973970432016, -4.894125840469273570, -1.768604793866979108E-15 ) ) ;
#536=AXIS2_PLACEMENT_3D ( 'NONE', #63748, #14905, #19454 ) ;
#556=LINE ( 'NONE', #57031, #55928 ) ;
#642=ORIENTED_EDGE ( 'NONE', *, *, #21432, .T. ) ;
#744=CARTESIAN_POINT ( 'NONE',  ( -7.794228634059950700, -4.500000000000003553, 0.000000000000000000 ) ) ;
#861=CARTESIAN_POINT ( 'NONE',  ( -3.535366420403587284, 9.000000000000008882, 0.6617903051486830890 ) ) ;
#1029=EDGE_LOOP ( 'NONE', ( #6531, #47187, #15663, #64925, #17552 ) ) ;
#1076=CARTESIAN_POINT ( 'NONE',  ( 7.335726704534227594, 5.294148637306920868, 0.03572125916566718656 ) ) ;
#1144=PRODUCT_DEFINITION_FORMATION_WITH_SPECIFIED_SOURCE ( 'ANY', '', #64784, .NOT_KNOWN. ) ;
#1202=ORIENTED_EDGE ( 'NONE', *, *, #65528, .F. ) ;
#1263=FILL_AREA_STYLE ('',( #17201 ) ) ;
#1292=ORIENTED_EDGE ( 'NONE', *, *, #37976, .F. ) ;
#1317=ORIENTED_EDGE ( 'NONE', *, *, #27225, .T. ) ;
#1320=CARTESIAN_POINT ( 'NONE',  ( 0.9115210089146362771, 9.000000000000010658, 3.505587024369798722E-15 ) ) ;
#1372=DIRECTION ( 'NONE',  ( -0.7071067811865487940, 0.000000000000000000, 0.7071067811865463515 ) ) ;
#1402=COLOUR_RGB ( '', 0.40784314, 0.44705882, 0.49803922) ;
#1588=CARTESIAN_POINT ( 'NONE',  ( -1.805736402306164390, 9.000000000000007105, 0.1687517039304846367 ) ) ;
#1736=DIRECTION ( 'NONE',  ( -0.8660254037844385966, -0.5000000000000002220, 0.000000000000000000 ) ) ;
#1765=DIRECTION ( 'NONE',  ( 0.5000000000000001110, 0.8660254037844384856, 0.000000000000000000 ) ) ;
#1776=EDGE_CURVE ( 'NONE', #32384, #10461, #7100, .T. ) ;
#1944=SURFACE_SIDE_STYLE ('',( #33344 ) ) ;
#1966=ORIENTED_EDGE ( 'NONE', *, *, #12053, .T. ) ;
#2043=AXIS2_PLACEMENT_3D ( 'NONE', #5876, #47475, #15779 ) ;
#2124=AXIS2_PLACEMENT_3D ( 'NONE', #34381, #27684, #22795 ) ;
#2163=ORIENTED_EDGE ( 'NONE', *, *, #27689, .T. ) ;
#2274=VERTEX_POINT ( 'NONE', #45287 ) ;
#2276=CARTESIAN_POINT ( 'NONE',  ( -8.252730563585677359, 3.705851362693089346, 0.03572125916567089887 ) ) ;
#2342=CARTESIAN_POINT ( 'NONE',  ( -8.690363669209109077, -2.947848588679142789, 0.1381979515792671198 ) ) ;
#2375=AXIS2_PLACEMENT_3D ( 'NONE', #25103, #46616, #57461 ) ;
#2407=CARTESIAN_POINT ( 'NONE',  ( 0.000000000000000000, 0.000000000000000000, 0.2499999999999924227 ) ) ;
#2904=EDGE_CURVE ( 'NONE', #31954, #32384, #62599, .T. ) ;
#3113=ORIENTED_EDGE ( 'NONE', *, *, #19765, .F. ) ;
#3293=CYLINDRICAL_SURFACE ( 'NONE', #37630, 7.500000000000000000 ) ;
#3314=VERTEX_POINT ( 'NONE', #33972 ) ;
#3343=CARTESIAN_POINT ( 'NONE',  ( 5.196152422706629359, 9.000000000000008882, 7.500000000000000000 ) ) ;
#3436=CONICAL_SURFACE ( 'NONE', #41741, 9.000000000000007105, 0.7853981633974500554 ) ;
#3464=DIRECTION ( 'NONE',  ( 0.000000000000000000, 0.000000000000000000, -1.000000000000000000 ) ) ;
#3472=CIRCLE ( 'NONE', #67544, 5.000000000000000000 ) ;
#3538=VECTOR ( 'NONE', #10938, 1000.000000000000227 ) ;
#3599=PLANE ( 'NONE',  #2375 ) ;
#3618=CARTESIAN_POINT ( 'NONE',  ( 8.701243704650558186, -2.929003814506409675, 0.1702817813269560110 ) ) ;
#3774=EDGE_CURVE ( 'NONE', #40384, #12618, #42438, .T. ) ;
#3857=AXIS2_PLACEMENT_3D ( 'NONE', #51199, #63482, #20206 ) ;
#3955=DIRECTION ( 'NONE',  ( 0.5000000000000001110, -0.8660254037844384856, 0.000000000000000000 ) ) ;
#4038=DIRECTION ( 'NONE',  ( 0.000000000000000000, 0.000000000000000000, 1.000000000000000000 ) ) ;
#4058=FILL_AREA_STYLE ('',( #67759 ) ) ;
#4116=DIRECTION ( 'NONE',  ( -1.224646799147353207E-16, 1.000000000000000000, 0.000000000000000000 ) ) ;
#4302=DIRECTION ( 'NONE',  ( 0.000000000000000000, 0.000000000000000000, 1.000000000000000000 ) ) ;
#4628=ORIENTED_EDGE ( 'NONE', *, *, #20178, .F. ) ;
#4690=ORIENTED_EDGE ( 'NONE', *, *, #60406, .T. ) ;
#4707=DIRECTION ( 'NONE',  ( -0.000000000000000000, -0.000000000000000000, 1.000000000000000000 ) ) ;
#4855=VERTEX_POINT ( 'NONE', #25438 ) ;
#4857=CARTESIAN_POINT ( 'NONE',  ( 10.39230484541327115, -3.482307324624967703E-15, 1.392304845413258718 ) ) ;
#4947=ORIENTED_EDGE ( 'NONE', *, *, #47798, .T. ) ;
#5072=ADVANCED_FACE ( 'NONE', ( #29843 ), #7358, .T. ) ;
#5194=CARTESIAN_POINT ( 'NONE',  ( 9.566487832665400148, 1.430357023834056385, 0.6362876910938520814 ) ) ;
#5382=CARTESIAN_POINT ( 'NONE',  ( -5.196152422706634688, -9.000000000000005329, 1.392304845413258052 ) ) ;
#5553=ORIENTED_EDGE ( 'NONE', *, *, #53824, .T. ) ;
#5650=EDGE_CURVE ( 'NONE', #12618, #7642, #13199, .T. ) ;
#5864=CARTESIAN_POINT ( 'NONE',  ( -0.9113929259990888321, 9.000000000000008882, 0.04319542563019723030 ) ) ;
#5872=ORIENTED_EDGE ( 'NONE', *, *, #64729, .T. ) ;
#5876=CARTESIAN_POINT ( 'NONE',  ( 0.000000000000000000, 0.000000000000000000, 0.000000000000000000 ) ) ;
#5939=ADVANCED_FACE ( 'NONE', ( #52668 ), #58629, .F. ) ;
#5976=VECTOR ( 'NONE', #39069, 1000.000000000000000 ) ;
#6111=EDGE_CURVE ( 'NONE', #29727, #3314, #19787, .T. ) ;
#6526=EDGE_LOOP ( 'NONE', ( #33985, #69508, #69587, #69521 ) ) ;
#6531=ORIENTED_EDGE ( 'NONE', *, *, #46388, .F. ) ;
#6613=DIRECTION ( 'NONE',  ( 0.000000000000000000, 0.000000000000000000, 1.000000000000000000 ) ) ;
#6644=CARTESIAN_POINT ( 'NONE',  ( 7.500000000000000000, 9.184850993605147944E-16, 1.000000000000000000 ) ) ;
#6690=LINE ( 'NONE', #50318, #11727 ) ;
#6746=ADVANCED_FACE ( 'NONE', ( #12593 ), #52148, .T. ) ;
#6790=ADVANCED_FACE ( 'NONE', ( #7342 ), #7665, .T. ) ;
#6852=AXIS2_PLACEMENT_3D ( 'NONE', #23761, #28675, #59654 ) ;
#6952=PRESENTATION_STYLE_ASSIGNMENT (( #7311 ) ) ;
#7100=LINE ( 'NONE', #56675, #69183 ) ;
#7217=DIRECTION ( 'NONE',  ( 0.000000000000000000, 0.000000000000000000, 1.000000000000000000 ) ) ;
#7311=SURFACE_STYLE_USAGE ( .BOTH. , #1944 ) ;
#7342=FACE_OUTER_BOUND ( 'NONE', #52596, .T. ) ;
#7358=CONICAL_SURFACE ( 'NONE', #54538, 9.000000000000007105, 0.7853981633974500554 ) ;
#7561=SHAPE_DEFINITION_REPRESENTATION ( #68685, #10054 ) ;
#7574=DIRECTION ( 'NONE',  ( -1.000000000000000000, 0.000000000000000000, 0.000000000000000000 ) ) ;
#7633=CARTESIAN_POINT ( 'NONE',  ( -9.000000000000007105, 0.000000000000000000, 0.000000000000000000 ) ) ;
#7642=VERTEX_POINT ( 'NONE', #16893 ) ;
#7649=CARTESIAN_POINT ( 'NONE',  ( 6.021969435454503028, -7.569642976165943615, 0.6362876910938544128 ) ) ;
#7665=PLANE ( 'NONE',  #45383 ) ;
#7822=( GEOMETRIC_REPRESENTATION_CONTEXT ( 3 ) GLOBAL_UNCERTAINTY_ASSIGNED_CONTEXT ( ( #18716 ) ) GLOBAL_UNIT_ASSIGNED_CONTEXT ( ( #55486, #23464, #39341 ) ) REPRESENTATION_CONTEXT ( 'NONE', 'WORKASPACE' ) );
#7898=CARTESIAN_POINT ( 'NONE',  ( 5.196152422706636465, -9.000000000000005329, 7.500000000000000000 ) ) ;
#7954=CONICAL_SURFACE ( 'NONE', #47322, 9.000000000000007105, 0.7853981633974500554 ) ;
#8008=ORIENTED_EDGE ( 'NONE', *, *, #62717, .T. ) ;
#8036=CARTESIAN_POINT ( 'NONE',  ( -10.39230484541327293, 3.364658241569156409E-15, 1.392304845413260939 ) ) ;
#8118=EDGE_CURVE ( 'NONE', #50919, #12618, #39845, .T. ) ;
#8120=DIRECTION ( 'NONE',  ( 1.000000000000000000, 0.000000000000000000, 0.000000000000000000 ) ) ;
#8332=SURFACE_SIDE_STYLE ('',( #18848 ) ) ;
#8354=DIRECTION ( 'NONE',  ( 1.000000000000000000, 0.000000000000000000, 0.000000000000000000 ) ) ;
#8365=AXIS2_PLACEMENT_3D ( 'NONE', #34642, #18489, #7574 ) ;
#8398=FACE_OUTER_BOUND ( 'NONE', #65119, .T. ) ;
#8527=FILL_AREA_STYLE ('',( #29962 ) ) ;
#8613=VERTEX_POINT ( 'NONE', #37173 ) ;
#8665=B_SPLINE_CURVE_WITH_KNOTS ( 'NONE', 3,
 ( #45996, #67419, #14942, #60565, #64828, #1076, #43763, #38500 ),
 .UNSPECIFIED., .F., .F.,
 ( 4, 2, 2, 4 ),
 ( 2.544313220902908671E-07, 0.002693395767724538360, 0.004039966435925761504, 0.005386537104126985082 ),
 .UNSPECIFIED. ) ;
#8680=CARTESIAN_POINT ( 'NONE',  ( -8.021777294149474713, 4.105874159530735312, 1.233279971202261294E-15 ) ) ;
#8693=CIRCLE ( 'NONE', #65970, 5.000000000000000000 ) ;
#8905=CIRCLE ( 'NONE', #30212, 7.749999999999993783 ) ;
#8982=CARTESIAN_POINT ( 'NONE',  ( 0.000000000000000000, -9.000000000000007105, 0.000000000000000000 ) ) ;
#8985=ORIENTED_EDGE ( 'NONE', *, *, #58452, .T. ) ;
#9094=DIRECTION ( 'NONE',  ( -0.000000000000000000, -0.000000000000000000, -1.000000000000000000 ) ) ;
#9127=AXIS2_PLACEMENT_3D ( 'NONE', #41686, #10346, #8354 ) ;
#9151=DIRECTION ( 'NONE',  ( -0.5000000000000002220, 0.8660254037844385966, 0.000000000000000000 ) ) ;
#9203=ORIENTED_EDGE ( 'NONE', *, *, #19941, .F. ) ;
#9294=ORIENTED_EDGE ( 'NONE', *, *, #20178, .T. ) ;
#9306=AXIS2_PLACEMENT_3D ( 'NONE', #48147, #59323, #32598 ) ;
#9378=CONICAL_SURFACE ( 'NONE', #45347, 7.500000000000000000, 0.7853981633974518317 ) ;
#9474=AXIS2_PLACEMENT_3D ( 'NONE', #26283, #25583, #15766 ) ;
#9577=ORIENTED_EDGE ( 'NONE', *, *, #28226, .T. ) ;
#9627=PLANE ( 'NONE',  #536 ) ;
#9798=CARTESIAN_POINT ( 'NONE',  ( -5.196152422706634688, 9.000000000000008882, 1.392304845413263159 ) ) ;
#9896=B_SPLINE_CURVE_WITH_KNOTS ( 'NONE', 3,
 ( #23863, #55876, #2342, #18246, #45713, #8036 ),
 .UNSPECIFIED., .F., .F.,
 ( 4, 2, 4 ),
 ( 0.005386537104126978143, 0.008060814333094822037, 0.01073509156206266593 ),
 .UNSPECIFIED. ) ;
#10054=SHAPE_REPRESENTATION ( '10. Bolt M10x25', ( #42840 ), #29323 ) ;
#10129=CYLINDRICAL_SURFACE ( 'NONE', #9474, 5.000000000000000000 ) ;
#10180=LINE ( 'NONE', #20376, #23939 ) ;
#10228=DIRECTION ( 'NONE',  ( 1.000000000000000000, 0.000000000000000000, 0.000000000000000000 ) ) ;
#10254=VECTOR ( 'NONE', #18873, 1000.000000000000000 ) ;
#10294=UNCERTAINTY_MEASURE_WITH_UNIT (LENGTH_MEASURE( 1.000000000000000082E-05 ), #34192, 'distance_accuracy_value', 'NONE');
#10346=DIRECTION ( 'NONE',  ( 0.000000000000000000, 0.000000000000000000, 1.000000000000000000 ) ) ;
#10461=VERTEX_POINT ( 'NONE', #27978 ) ;
#10524=ORIENTED_EDGE ( 'NONE', *, *, #8118, .T. ) ;
#10594=AXIS2_PLACEMENT_3D ( 'NONE', #65572, #59592, #38887 ) ;
#10690=AXIS2_PLACEMENT_3D ( 'NONE', #64982, #69578, #16837 ) ;
#10890=CARTESIAN_POINT ( 'NONE',  ( 3.108481029118200567, -9.000000000000003553, 0.5125184569636065390 ) ) ;
#10938=DIRECTION ( 'NONE',  ( -0.5000000000000001110, -0.8660254037844384856, 0.000000000000000000 ) ) ;
#11029=EDGE_CURVE ( 'NONE', #10461, #50919, #22192, .T. ) ;
#11300=CONICAL_SURFACE ( 'NONE', #66372, 9.000000000000007105, 0.7853981633974500554 ) ;
#11681=ADVANCED_FACE ( 'NONE', ( #51851 ), #3599, .T. ) ;
#11703=STYLED_ITEM ( 'NONE', ( #25523 ), #26844 ) ;
#11727=VECTOR ( 'NONE', #21856, 1000.000000000000000 ) ;
#11757=EDGE_CURVE ( 'NONE', #31954, #33911, #27503, .T. ) ;
#11889=CARTESIAN_POINT ( 'NONE',  ( -5.000000000000000000, 0.000000000000000000, 42.50000000000000000 ) ) ;
#12011=ORIENTED_EDGE ( 'NONE', *, *, #62267, .T. ) ;
#12051=DIRECTION ( 'NONE',  ( 1.000000000000000000, 0.000000000000000000, 0.000000000000000000 ) ) ;
#12053=EDGE_CURVE ( 'NONE', #44244, #17222, #35935, .T. ) ;
#12089=ORIENTED_EDGE ( 'NONE', *, *, #60406, .F. ) ;
#12258=CARTESIAN_POINT ( 'NONE',  ( 4.793647677013320951, 9.000000000000008882, 1.191052472566604292 ) ) ;
#12593=FACE_OUTER_BOUND ( 'NONE', #57267, .T. ) ;
#12618=VERTEX_POINT ( 'NONE', #62125 ) ;
#12620=DIRECTION ( 'NONE',  ( 0.000000000000000000, 0.000000000000000000, 1.000000000000000000 ) ) ;
#12920=ORIENTED_EDGE ( 'NONE', *, *, #59354, .T. ) ;
#12968=CARTESIAN_POINT ( 'NONE',  ( 3.108481029118195238, 9.000000000000007105, 0.5125184569636095366 ) ) ;
#13069=DIRECTION ( 'NONE',  ( 0.000000000000000000, 0.000000000000000000, -1.000000000000000000 ) ) ;
#13096=ORIENTED_EDGE ( 'NONE', *, *, #26530, .F. ) ;
#13195=B_SPLINE_CURVE_WITH_KNOTS ( 'NONE', 3,
 ( #62610, #40164, #66882, #14426, #67559, #29574, #35899, #62278, #45790, #14106, #35563, #19716 ),
 .UNSPECIFIED., .F., .F.,
 ( 4, 2, 2, 2, 2, 4 ),
 ( 0.01082081597914125344, 0.01149352919195929454, 0.01216624240477733390, 0.01351166883041341610, 0.01485709525604949656, 0.01620252168168557702 ),
 .UNSPECIFIED. ) ;
#13199=B_SPLINE_CURVE_WITH_KNOTS ( 'NONE', 3,
 ( #66401, #55141, #49905, #7649, #60420, #60089 ),
 .UNSPECIFIED., .F., .F.,
 ( 4, 2, 4 ),
 ( 0.005386537104126976408, 0.008060814333094815098, 0.01073509156206265552 ),
 .UNSPECIFIED. ) ;
#13382=DIRECTION ( 'NONE',  ( -0.000000000000000000, -0.000000000000000000, -1.000000000000000000 ) ) ;
#13408=FILL_AREA_STYLE_COLOUR ( '', #1402 ) ;
#13620=VECTOR ( 'NONE', #32807, 1000.000000000000000 ) ;
#13653=DIRECTION ( 'NONE',  ( -1.000000000000000000, 0.000000000000000000, 0.000000000000000000 ) ) ;
#13706=ADVANCED_BREP_SHAPE_REPRESENTATION ( '', ( #26844, #42840 ), #29323 ) ;
#13790=PRESENTATION_STYLE_ASSIGNMENT (( #14471 ) ) ;
#14011=CARTESIAN_POINT ( 'NONE',  ( 0.000000000000000000, 0.000000000000000000, 0.000000000000000000 ) ) ;
#14014=LINE ( 'NONE', #24209, #56335 ) ;
#14078=DIRECTION ( 'NONE',  ( -1.000000000000000000, 0.000000000000000000, 0.000000000000000000 ) ) ;
#14106=CARTESIAN_POINT ( 'NONE',  ( -4.377616827404060551, -9.000000000000007105, 1.000745235317158643 ) ) ;
#14146=VECTOR ( 'NONE', #67902, 1000.000000000000000 ) ;
#14164=EDGE_LOOP ( 'NONE', ( #38074, #68269, #24095, #53454, #1292, #44530, #41118 ) ) ;
#14209=B_SPLINE_CURVE_WITH_KNOTS ( 'NONE', 3,
 ( #64289, #30892, #52718, #5194, #26636, #4857 ),
 .UNSPECIFIED., .F., .F.,
 ( 4, 2, 4 ),
 ( 0.005386537104126985082, 0.008060814333094825507, 0.01073509156206266767 ),
 .UNSPECIFIED. ) ;
#14384=ORIENTED_EDGE ( 'NONE', *, *, #26530, .T. ) ;
#14426=CARTESIAN_POINT ( 'NONE',  ( -0.9113929259990886100, -9.000000000000001776, 0.04319542563019202613 ) ) ;
#14471=SURFACE_STYLE_USAGE ( .BOTH. , #51780 ) ;
#14721=CARTESIAN_POINT ( 'NONE',  ( -6.898093598910799429, 6.052151411320864760, 0.1381979515792698954 ) ) ;
#14905=DIRECTION ( 'NONE',  ( 0.8660254037844385966, -0.5000000000000002220, 0.000000000000000000 ) ) ;
#14923=CLOSED_SHELL ( 'NONE', ( #28952, #60140, #58083, #64777, #41995, #50849, #5939, #39263, #42582, #27762, #31837, #55988, #62658, #6790, #5072, #59971, #45411, #17725, #6746, #56080, #15442, #62192, #11681, #61443, #51663 ) ) ;
#14942=CARTESIAN_POINT ( 'NONE',  ( 6.020204320972965206, 7.572700244129134894, 0.6386920474458019914 ) ) ;
#14994=PLANE ( 'NONE',  #21785 ) ;
#15312=CARTESIAN_POINT ( 'NONE',  ( 0.000000000000000000, 0.000000000000000000, 0.7500000000000000000 ) ) ;
#15442=ADVANCED_FACE ( 'NONE', ( #39420, #48948 ), #23216, .F. ) ;
#15509=DIRECTION ( 'NONE',  ( 1.000000000000000000, 0.000000000000000000, 0.000000000000000000 ) ) ;
#15663=ORIENTED_EDGE ( 'NONE', *, *, #2904, .F. ) ;
#15766=DIRECTION ( 'NONE',  ( -1.000000000000000000, 0.000000000000000000, 0.000000000000000000 ) ) ;
#15779=DIRECTION ( 'NONE',  ( 1.000000000000000000, 0.000000000000000000, 0.000000000000000000 ) ) ;
#15815=VECTOR ( 'NONE', #41942, 1000.000000000000000 ) ;
#15822=ORIENTED_EDGE ( 'NONE', *, *, #22287, .F. ) ;
#16387=VERTEX_POINT ( 'NONE', #23905 ) ;
#16505=PLANE ( 'NONE',  #10690 ) ;
#16826=VERTEX_POINT ( 'NONE', #7633 ) ;
#16837=DIRECTION ( 'NONE',  ( -0.5000000000000001110, 0.8660254037844384856, 0.000000000000000000 ) ) ;
#16884=CARTESIAN_POINT ( 'NONE',  ( 4.383403428314272432, -9.000000000000005329, 1.003298500868273102 ) ) ;
#16893=CARTESIAN_POINT ( 'NONE',  ( 5.196152422706636465, -9.000000000000005329, 1.392304845413258274 ) ) ;
#16947=DIRECTION ( 'NONE',  ( 0.5000000000000001110, -0.8660254037844384856, 0.000000000000000000 ) ) ;
#17001=B_SPLINE_CURVE_WITH_KNOTS ( 'NONE', 3,
 ( #39395, #1320, #60453, #12968, #56217, #66437, #12258, #33725 ),
 .UNSPECIFIED., .F., .F.,
 ( 4, 2, 2, 4 ),
 ( 0.01337289451763051980, 0.01607096743472092790, 0.01742000389326613108, 0.01876904035181133773 ),
 .UNSPECIFIED. ) ;
#17007=MECHANICAL_DESIGN_GEOMETRIC_PRESENTATION_REPRESENTATION('',(#38380),#55024);
#17131=EDGE_CURVE ( 'NONE', #60346, #29727, #3472, .T. ) ;
#17201=FILL_AREA_STYLE_COLOUR ( '', #68494 ) ;
#17203=EDGE_CURVE ( 'NONE', #35681, #47180, #39507, .T. ) ;
#17222=VERTEX_POINT ( 'NONE', #46982 ) ;
#17303=CARTESIAN_POINT ( 'NONE',  ( -9.000000000000007105, 0.000000000000000000, 0.000000000000000000 ) ) ;
#17346=FACE_OUTER_BOUND ( 'NONE', #20407, .T. ) ;
#17506=CARTESIAN_POINT ( 'NONE',  ( -3.109213548236402502, 9.000000000000007105, 0.5129086262188717882 ) ) ;
#17545=ORIENTED_EDGE ( 'NONE', *, *, #11757, .F. ) ;
#17552=ORIENTED_EDGE ( 'NONE', *, *, #55130, .F. ) ;
#17687=SURFACE_STYLE_USAGE ( .BOTH. , #66903 ) ;
#17725=ADVANCED_FACE ( 'NONE', ( #33404 ), #11300, .T. ) ;
#17872=DIRECTION ( 'NONE',  ( 1.000000000000000000, 0.000000000000000000, 0.000000000000000000 ) ) ;
#17894=CARTESIAN_POINT ( 'NONE',  ( 0.000000000000000000, 0.000000000000000000, 0.000000000000000000 ) ) ;
#17918=DIRECTION ( 'NONE',  ( -1.000000000000000000, 0.000000000000000000, 0.000000000000000000 ) ) ;
#18246=CARTESIAN_POINT ( 'NONE',  ( -9.566487832665407254, -1.430357023834055719, 0.6362876910938550790 ) ) ;
#18489=DIRECTION ( 'NONE',  ( -0.000000000000000000, -0.000000000000000000, 1.000000000000000000 ) ) ;
#18575=EDGE_LOOP ( 'NONE', ( #59972, #38810, #12011, #38539 ) ) ;
#18583=EDGE_LOOP ( 'NONE', ( #33606, #17545, #45797, #30336, #57862 ) ) ;
#18598=CARTESIAN_POINT ( 'NONE',  ( 0.000000000000000000, 0.000000000000000000, 42.50000000000000000 ) ) ;
#18670=DIRECTION ( 'NONE',  ( -1.000000000000000000, 0.000000000000000000, 0.000000000000000000 ) ) ;
#18716=UNCERTAINTY_MEASURE_WITH_UNIT (LENGTH_MEASURE( 1.000000000000000082E-05 ), #55486, 'distance_accuracy_value', 'NONE');
#18848=SURFACE_STYLE_FILL_AREA ( #4058 ) ;
#18868=DIRECTION ( 'NONE',  ( 0.000000000000000000, 0.000000000000000000, 1.000000000000000000 ) ) ;
#18873=DIRECTION ( 'NONE',  ( -0.000000000000000000, -0.000000000000000000, -1.000000000000000000 ) ) ;
#18944=AXIS2_PLACEMENT_3D ( 'NONE', #50034, #65492, #54589 ) ;
#18962=DIRECTION ( 'NONE',  ( -0.000000000000000000, -0.000000000000000000, -1.000000000000000000 ) ) ;
#19136=EDGE_CURVE ( 'NONE', #4855, #3314, #60936, .T. ) ;
#19185=CIRCLE ( 'NONE', #6852, 7.249999999999999112 ) ;
#19404=( LENGTH_UNIT ( ) NAMED_UNIT ( * ) SI_UNIT ( .MILLI., .METRE. ) );
#19450=PLANE ( 'NONE',  #68353 ) ;
#19454=DIRECTION ( 'NONE',  ( 0.5000000000000001110, 0.8660254037844384856, 0.000000000000000000 ) ) ;
#19716=CARTESIAN_POINT ( 'NONE',  ( -5.196152422706634688, -9.000000000000005329, 1.392304845413258052 ) ) ;
#19765=EDGE_CURVE ( 'NONE', #17222, #28040, #8905, .T. ) ;
#19787=LINE ( 'NONE', #31027, #32942 ) ;
#19934=CARTESIAN_POINT ( 'NONE',  ( 0.000000000000000000, 0.000000000000000000, 0.2499999999999924227 ) ) ;
#19941=EDGE_CURVE ( 'NONE', #2274, #50919, #14209, .T. ) ;
#20178=EDGE_CURVE ( 'NONE', #27375, #27464, #20939, .T. ) ;
#20206=DIRECTION ( 'NONE',  ( 1.000000000000000000, 0.000000000000000000, 0.000000000000000000 ) ) ;
#20376=CARTESIAN_POINT ( 'NONE',  ( 10.39230484541327115, -4.119968255444916849E-15, 7.500000000000000000 ) ) ;
#20407=EDGE_LOOP ( 'NONE', ( #35403, #42842, #23723, #30877 ) ) ;
#20421=EDGE_LOOP ( 'NONE', ( #41793, #59416, #3113, #67996 ) ) ;
#20504=LINE ( 'NONE', #67654, #54526 ) ;
#20939=B_SPLINE_CURVE_WITH_KNOTS ( 'NONE', 3,
 ( #35416, #23449, #44956, #66362, #56866, #2276, #8680, #55814 ),
 .UNSPECIFIED., .F., .F.,
 ( 4, 2, 2, 4 ),
 ( 2.544313220891868126E-07, 0.002693395767724533589, 0.004039966435925756300, 0.005386537104126978143 ),
 .UNSPECIFIED. ) ;
#21099=CARTESIAN_POINT ( 'NONE',  ( 0.000000000000000000, 0.000000000000000000, 0.000000000000000000 ) ) ;
#21432=EDGE_CURVE ( 'NONE', #65961, #28130, #25048, .T. ) ;
#21785=AXIS2_PLACEMENT_3D ( 'NONE', #37156, #4038, #32181 ) ;
#21792=EDGE_LOOP ( 'NONE', ( #23084, #66700, #25087, #26143 ) ) ;
#21856=DIRECTION ( 'NONE',  ( -0.000000000000000000, -0.000000000000000000, -1.000000000000000000 ) ) ;
#21986=EDGE_LOOP ( 'NONE', ( #33609, #37773, #5872 ) ) ;
#22171=DIRECTION ( 'NONE',  ( 1.000000000000000000, 0.000000000000000000, -0.000000000000000000 ) ) ;
#22189=LINE ( 'NONE', #43687, #3538 ) ;
#22192=LINE ( 'NONE', #38760, #35952 ) ;
#22287=EDGE_CURVE ( 'NONE', #44244, #16387, #56360, .T. ) ;
#22301=B_SPLINE_CURVE_WITH_KNOTS ( 'NONE', 3,
 ( #5382, #52, #27178, #26505, #48714, #48028, #416, #744 ),
 .UNSPECIFIED., .F., .F.,
 ( 4, 2, 2, 4 ),
 ( 2.544313220903533887E-07, 0.002693395767724534023, 0.004039966435925756300, 0.005386537104126978143 ),
 .UNSPECIFIED. ) ;
#22521=CARTESIAN_POINT ( 'NONE',  ( 0.000000000000000000, 0.000000000000000000, 0.000000000000000000 ) ) ;
#22795=DIRECTION ( 'NONE',  ( -1.000000000000000000, 0.000000000000000000, 0.000000000000000000 ) ) ;
#22835=CARTESIAN_POINT ( 'NONE',  ( 4.793647677013328057, -9.000000000000007105, 1.191052472566601628 ) ) ;
#22914=ORIENTED_EDGE ( 'NONE', *, *, #1776, .T. ) ;
#22944=ORIENTED_EDGE ( 'NONE', *, *, #39429, .T. ) ;
#23084=ORIENTED_EDGE ( 'NONE', *, *, #60494, .F. ) ;
#23113=CARTESIAN_POINT ( 'NONE',  ( -0.4573008633723372740, 9.000000000000007105, 0.008766315107681324145 ) ) ;
#23216=PLANE ( 'NONE',  #58458 ) ;
#23233=CARTESIAN_POINT ( 'NONE',  ( 5.000000000000000000, 6.123233995736766282E-16, 42.50000000000000000 ) ) ;
#23286=SURFACE_STYLE_FILL_AREA ( #55286 ) ;
#23449=CARTESIAN_POINT ( 'NONE',  ( -9.984889265949535186, 0.7056644834263136046, 0.9848892659495233071 ) ) ;
#23464=( NAMED_UNIT ( * ) PLANE_ANGLE_UNIT ( ) SI_UNIT ( $, .RADIAN. ) );
#23723=ORIENTED_EDGE ( 'NONE', *, *, #19136, .T. ) ;
#23737=DIRECTION ( 'NONE',  ( 0.000000000000000000, 0.000000000000000000, 1.000000000000000000 ) ) ;
#23761=CARTESIAN_POINT ( 'NONE',  ( 0.000000000000000000, 0.000000000000000000, 1.000000000000000000 ) ) ;
#23777=ORIENTED_EDGE ( 'NONE', *, *, #33823, .T. ) ;
#23786=CIRCLE ( 'NONE', #29402, 9.000000000000007105 ) ;
#23863=CARTESIAN_POINT ( 'NONE',  ( -7.794228634059950700, -4.500000000000003553, 0.000000000000000000 ) ) ;
#23905=CARTESIAN_POINT ( 'NONE',  ( 7.500000000000000000, 9.184850993605147944E-16, 0.2499999999999924227 ) ) ;
#23939=VECTOR ( 'NONE', #9151, 999.9999999999998863 ) ;
#24000=VECTOR ( 'NONE', #36268, 1000.000000000000000 ) ;
#24013=ORIENTED_EDGE ( 'NONE', *, *, #62717, .F. ) ;
#24016=ORIENTED_EDGE ( 'NONE', *, *, #2904, .T. ) ;
#24043=ORIENTED_EDGE ( 'NONE', *, *, #39429, .F. ) ;
#24095=ORIENTED_EDGE ( 'NONE', *, *, #3774, .F. ) ;
#24209=CARTESIAN_POINT ( 'NONE',  ( -10.39230484541327293, 3.469446951953614189E-15, 7.500000000000000000 ) ) ;
#24276=CARTESIAN_POINT ( 'NONE',  ( 0.000000000000000000, 0.000000000000000000, 0.000000000000000000 ) ) ;
#24348=VERTEX_POINT ( 'NONE', #59581 ) ;
#24542=CARTESIAN_POINT ( 'NONE',  ( -7.342319042881619851, 5.282730372348555470, 1.478919525906007998E-15 ) ) ;
#24754=ORIENTED_EDGE ( 'NONE', *, *, #31000, .T. ) ;
#24844=UNCERTAINTY_MEASURE_WITH_UNIT (LENGTH_MEASURE( 1.000000000000000082E-05 ), #65869, 'distance_accuracy_value', 'NONE');
#25034=( NAMED_UNIT ( * ) PLANE_ANGLE_UNIT ( ) SI_UNIT ( $, .RADIAN. ) );
#25048=LINE ( 'NONE', #46559, #31503 ) ;
#25087=ORIENTED_EDGE ( 'NONE', *, *, #6111, .T. ) ;
#25103=CARTESIAN_POINT ( 'NONE',  ( 0.000000000000000000, 0.000000000000000000, 1.000000000000000000 ) ) ;
#25125=ORIENTED_EDGE ( 'NONE', *, *, #25242, .F. ) ;
#25242=EDGE_CURVE ( 'NONE', #58823, #27375, #14014, .T. ) ;
#25438=CARTESIAN_POINT ( 'NONE',  ( 5.000000000000000000, 6.123233995736766282E-16, 7.500000000000000000 ) ) ;
#25523=PRESENTATION_STYLE_ASSIGNMENT (( #30101 ) ) ;
#25541=LINE ( 'NONE', #47056, #10254 ) ;
#25583=DIRECTION ( 'NONE',  ( -0.000000000000000000, -0.000000000000000000, -1.000000000000000000 ) ) ;
#26143=ORIENTED_EDGE ( 'NONE', *, *, #65528, .T. ) ;
#26147=AXIS2_PLACEMENT_3D ( 'NONE', #50038, #13069, #29597 ) ;
#26190=VECTOR ( 'NONE', #1372, 1000.000000000000000 ) ;
#26254=COLOUR_RGB ( '', 0.09019608, 0.27058824, 0.51372549) ;
#26283=CARTESIAN_POINT ( 'NONE',  ( 0.000000000000000000, 0.000000000000000000, 42.50000000000000000 ) ) ;
#26292=EDGE_CURVE ( 'NONE', #47180, #16387, #55548, .T. ) ;
#26379=CARTESIAN_POINT ( 'NONE',  ( -7.500000000000000000, 0.000000000000000000, 1.000000000000000000 ) ) ;
#26428=EDGE_LOOP ( 'NONE', ( #14384, #36204 ) ) ;
#26505=CARTESIAN_POINT ( 'NONE',  ( -6.667623377008404795, -6.451337545287478825, 0.2685431138779681981 ) ) ;
#26530=EDGE_CURVE ( 'NONE', #24348, #57711, #59954, .T. ) ;
#26636=CARTESIAN_POINT ( 'NONE',  ( 9.985360875542992787, 0.7048476316490956961, 0.9853608755428859833 ) ) ;
#26694=ORIENTED_EDGE ( 'NONE', *, *, #45647, .F. ) ;
#26844=MANIFOLD_SOLID_BREP ( 'Fillet1', #14923 ) ;
#26964=DIRECTION ( 'NONE',  ( -1.000000000000000000, 0.000000000000000000, 0.000000000000000000 ) ) ;
#26983=FACE_OUTER_BOUND ( 'NONE', #18583, .T. ) ;
#27032=CARTESIAN_POINT ( 'NONE',  ( 3.542013698345610972, -9.000000000000003553, 0.6642442188400904390 ) ) ;
#27142=EDGE_CURVE ( 'NONE', #24348, #35681, #31935, .T. ) ;
#27178=CARTESIAN_POINT ( 'NONE',  ( -6.020204320972967871, -7.572700244129130454, 0.6386920474458009922 ) ) ;
#27225=EDGE_CURVE ( 'NONE', #28040, #17222, #27443, .T. ) ;
#27313=CARTESIAN_POINT ( 'NONE',  ( -5.196152422706634688, 9.000000000000008882, 7.500000000000000000 ) ) ;
#27375=VERTEX_POINT ( 'NONE', #33747 ) ;
#27443=CIRCLE ( 'NONE', #48856, 7.749999999999993783 ) ;
#27464=VERTEX_POINT ( 'NONE', #40444 ) ;
#27503=LINE ( 'NONE', #58851, #13620 ) ;
#27684=DIRECTION ( 'NONE',  ( 0.000000000000000000, 0.000000000000000000, -1.000000000000000000 ) ) ;
#27689=EDGE_CURVE ( 'NONE', #58823, #31954, #20504, .T. ) ;
#27762=ADVANCED_FACE ( 'NONE', ( #46235 ), #9627, .F. ) ;
#27785=AXIS2_PLACEMENT_3D ( 'NONE', #38027, #58404, #10228 ) ;
#27903=FACE_OUTER_BOUND ( 'NONE', #43016, .T. ) ;
#27978=CARTESIAN_POINT ( 'NONE',  ( 10.39230484541327115, -4.119968255444916849E-15, 7.500000000000000000 ) ) ;
#28040=VERTEX_POINT ( 'NONE', #35914 ) ;
#28130=VERTEX_POINT ( 'NONE', #59408 ) ;
#28226=EDGE_CURVE ( 'NONE', #37986, #66051, #17001, .T. ) ;
#28344=CARTESIAN_POINT ( 'NONE',  ( -4.792168507806671585, 9.000000000000008882, 1.190312887963165922 ) ) ;
#28675=DIRECTION ( 'NONE',  ( 0.000000000000000000, 0.000000000000000000, -1.000000000000000000 ) ) ;
#28780=ORIENTED_EDGE ( 'NONE', *, *, #11029, .T. ) ;
#28952=ADVANCED_FACE ( 'NONE', ( #29944 ), #65477, .F. ) ;
#28968=DIRECTION ( 'NONE',  ( 0.000000000000000000, 0.000000000000000000, -1.000000000000000000 ) ) ;
#29089=EDGE_LOOP ( 'NONE', ( #58347, #15822, #1966, #64459 ) ) ;
#29178=DIRECTION ( 'NONE',  ( 0.000000000000000000, 0.000000000000000000, -1.000000000000000000 ) ) ;
#29232=ORIENTED_EDGE ( 'NONE', *, *, #59974, .F. ) ;
#29323=( GEOMETRIC_REPRESENTATION_CONTEXT ( 3 ) GLOBAL_UNCERTAINTY_ASSIGNED_CONTEXT ( ( #24844 ) ) GLOBAL_UNIT_ASSIGNED_CONTEXT ( ( #65869, #46180, #34537 ) ) REPRESENTATION_CONTEXT ( 'NONE', 'WORKASPACE' ) );
#29402=AXIS2_PLACEMENT_3D ( 'NONE', #56288, #66871, #8120 ) ;
#29574=CARTESIAN_POINT ( 'NONE',  ( -1.805736402306165722, -9.000000000000007105, 0.1687517039304795019 ) ) ;
#29597=DIRECTION ( 'NONE',  ( -1.000000000000000000, 0.000000000000000000, 0.000000000000000000 ) ) ;
#29615=CIRCLE ( 'NONE', #68950, 9.000000000000007105 ) ;
#29627=EDGE_LOOP ( 'NONE', ( #24013, #13096, #64089, #29906 ) ) ;
#29696=CIRCLE ( 'NONE', #8365, 7.500000000000000000 ) ;
#29727=VERTEX_POINT ( 'NONE', #11889 ) ;
#29775=( LENGTH_UNIT ( ) NAMED_UNIT ( * ) SI_UNIT ( .MILLI., .METRE. ) );
#29843=FACE_OUTER_BOUND ( 'NONE', #64053, .T. ) ;
#29906=ORIENTED_EDGE ( 'NONE', *, *, #48477, .F. ) ;
#29944=FACE_OUTER_BOUND ( 'NONE', #59563, .T. ) ;
#29962=FILL_AREA_STYLE_COLOUR ( '', #68668 ) ;
#30060=EDGE_LOOP ( 'NONE', ( #4628, #25125, #12089, #642, #66353 ) ) ;
#30064=DIRECTION ( 'NONE',  ( -0.000000000000000000, -0.000000000000000000, -1.000000000000000000 ) ) ;
#30101=SURFACE_STYLE_USAGE ( .BOTH. , #8332 ) ;
#30212=AXIS2_PLACEMENT_3D ( 'NONE', #52555, #4302, #39414 ) ;
#30220=CARTESIAN_POINT ( 'NONE',  ( 0.000000000000000000, 0.000000000000000000, 0.000000000000000000 ) ) ;
#30336=ORIENTED_EDGE ( 'NONE', *, *, #25242, .T. ) ;
#30467=EDGE_CURVE ( 'NONE', #16826, #27375, #65804, .T. ) ;
#30638=SHAPE_REPRESENTATION_RELATIONSHIP ( 'NONE' , 'NONE' ,  #10054, #13706 ) ;
#30758=FACE_OUTER_BOUND ( 'NONE', #6526, .T. ) ;
#30772=EDGE_CURVE ( 'NONE', #10461, #69624, #10180, .T. ) ;
#30877=ORIENTED_EDGE ( 'NONE', *, *, #6111, .F. ) ;
#30892=CARTESIAN_POINT ( 'NONE',  ( 8.246138225238285102, 3.717269627651449415, -3.339003878076450753E-15 ) ) ;
#31000=EDGE_CURVE ( 'NONE', #2274, #37986, #29615, .T. ) ;
#31027=CARTESIAN_POINT ( 'NONE',  ( -5.000000000000000000, 0.000000000000000000, 42.50000000000000000 ) ) ;
#31075=CARTESIAN_POINT ( 'NONE',  ( 7.794228634059951588, -4.500000000000003553, 0.000000000000000000 ) ) ;
#31318=DIRECTION ( 'NONE',  ( 0.7071067811865500152, 8.659560562354963673E-17, -0.7071067811865450192 ) ) ;
#31334=CIRCLE ( 'NONE', #2043, 9.000000000000007105 ) ;
#31364=DIRECTION ( 'NONE',  ( -0.000000000000000000, -0.000000000000000000, -1.000000000000000000 ) ) ;
#31415=TOROIDAL_SURFACE ( 'NONE', #2124, 7.249999999999999112, 0.2500000000000000000 ) ;
#31503=VECTOR ( 'NONE', #51103, 1000.000000000000000 ) ;
#31837=ADVANCED_FACE ( 'NONE', ( #26983 ), #16505, .F. ) ;
#31859=UNCERTAINTY_MEASURE_WITH_UNIT (LENGTH_MEASURE( 1.000000000000000082E-05 ), #19404, 'distance_accuracy_value', 'NONE');
#31883=DIRECTION ( 'NONE',  ( -0.5000000000000001110, -0.8660254037844384856, 0.000000000000000000 ) ) ;
#31901=AXIS2_PLACEMENT_3D ( 'NONE', #54948, #38843, #12051 ) ;
#31911=CONICAL_SURFACE ( 'NONE', #10594, 9.000000000000007105, 0.7853981633974500554 ) ;
#31935=CIRCLE ( 'NONE', #55537, 0.2500000000000000000 ) ;
#31954=VERTEX_POINT ( 'NONE', #34021 ) ;
#32181=DIRECTION ( 'NONE',  ( 1.000000000000000000, 0.000000000000000000, -0.000000000000000000 ) ) ;
#32332=CARTESIAN_POINT ( 'NONE',  ( 0.9115210089146371653, -9.000000000000005329, -1.741499739554841497E-15 ) ) ;
#32384=VERTEX_POINT ( 'NONE', #7898 ) ;
#32476=APPLICATION_CONTEXT ( 'automotive_design' ) ;
#32598=DIRECTION ( 'NONE',  ( 1.000000000000000000, 0.000000000000000000, 0.000000000000000000 ) ) ;
#32769=ORIENTED_EDGE ( 'NONE', *, *, #5650, .T. ) ;
#32807=DIRECTION ( 'NONE',  ( -0.000000000000000000, -0.000000000000000000, -1.000000000000000000 ) ) ;
#32942=VECTOR ( 'NONE', #31364, 1000.000000000000000 ) ;
#33056=MECHANICAL_DESIGN_GEOMETRIC_PRESENTATION_REPRESENTATION('',(#11703),#48803);
#33090=ORIENTED_EDGE ( 'NONE', *, *, #27142, .F. ) ;
#33344=SURFACE_STYLE_FILL_AREA ( #1263 ) ;
#33404=FACE_OUTER_BOUND ( 'NONE', #21986, .T. ) ;
#33606=ORIENTED_EDGE ( 'NONE', *, *, #33823, .F. ) ;
#33609=ORIENTED_EDGE ( 'NONE', *, *, #30467, .F. ) ;
#33725=CARTESIAN_POINT ( 'NONE',  ( 5.196152422706629359, 9.000000000000008882, 1.392304845413260272 ) ) ;
#33747=CARTESIAN_POINT ( 'NONE',  ( -10.39230484541327293, 3.364658241569156409E-15, 1.392304845413260939 ) ) ;
#33780=EDGE_LOOP ( 'NONE', ( #29232, #47828, #56458, #28780, #9203 ) ) ;
#33823=EDGE_CURVE ( 'NONE', #33911, #8613, #22301, .T. ) ;
#33855=CARTESIAN_POINT ( 'NONE',  ( -5.196152422706634688, -9.000000000000005329, 1.392304845413258052 ) ) ;
#33911=VERTEX_POINT ( 'NONE', #33855 ) ;
#33951=ORIENTED_EDGE ( 'NONE', *, *, #55130, .T. ) ;
#33972=CARTESIAN_POINT ( 'NONE',  ( -5.000000000000000000, 0.000000000000000000, 7.500000000000000000 ) ) ;
#33981=MECHANICAL_DESIGN_GEOMETRIC_PRESENTATION_REPRESENTATION('',(#68853),#34031);
#33985=ORIENTED_EDGE ( 'NONE', *, *, #26292, .F. ) ;
#34021=CARTESIAN_POINT ( 'NONE',  ( -5.196152422706633800, -9.000000000000005329, 7.500000000000000000 ) ) ;
#34031=( GEOMETRIC_REPRESENTATION_CONTEXT ( 3 ) GLOBAL_UNCERTAINTY_ASSIGNED_CONTEXT ( ( #10294 ) ) GLOBAL_UNIT_ASSIGNED_CONTEXT ( ( #34192, #51068, #40530 ) ) REPRESENTATION_CONTEXT ( 'NONE', 'WORKASPACE' ) );
#34063=DIRECTION ( 'NONE',  ( 0.000000000000000000, 0.000000000000000000, 1.000000000000000000 ) ) ;
#34092=CARTESIAN_POINT ( 'NONE',  ( 0.000000000000000000, 0.000000000000000000, 0.000000000000000000 ) ) ;
#34192=( LENGTH_UNIT ( ) NAMED_UNIT ( * ) SI_UNIT ( .MILLI., .METRE. ) );
#34301=CARTESIAN_POINT ( 'NONE',  ( 0.000000000000000000, 0.000000000000000000, 42.50000000000000000 ) ) ;
#34352=ORIENTED_EDGE ( 'NONE', *, *, #30467, .T. ) ;
#34381=CARTESIAN_POINT ( 'NONE',  ( 0.000000000000000000, 0.000000000000000000, 0.7500000000000000000 ) ) ;
#34537=( NAMED_UNIT ( * ) SI_UNIT ( $, .STERADIAN. ) SOLID_ANGLE_UNIT ( ) );
#34544=DIRECTION ( 'NONE',  ( 0.000000000000000000, 0.000000000000000000, -1.000000000000000000 ) ) ;
#34630=PRODUCT_CONTEXT ( 'NONE', #51410, 'mechanical' ) ;
#34642=CARTESIAN_POINT ( 'NONE',  ( 0.000000000000000000, 0.000000000000000000, 0.7500000000000000000 ) ) ;
#34897=CARTESIAN_POINT ( 'NONE',  ( 0.000000000000000000, 0.000000000000000000, 0.2499999999999924227 ) ) ;
#35067=DIRECTION ( 'NONE',  ( -1.000000000000000000, 0.000000000000000000, 0.000000000000000000 ) ) ;
#35403=ORIENTED_EDGE ( 'NONE', *, *, #17131, .F. ) ;
#35407=CARTESIAN_POINT ( 'NONE',  ( 5.196152422706629359, 9.000000000000008882, 1.392304845413260272 ) ) ;
#35416=CARTESIAN_POINT ( 'NONE',  ( -10.39230484541327293, 3.364658241569156409E-15, 1.392304845413260939 ) ) ;
#35561=DIRECTION ( 'NONE',  ( -1.000000000000000000, 0.000000000000000000, 0.000000000000000000 ) ) ;
#35563=CARTESIAN_POINT ( 'NONE',  ( -4.792168507806670696, -9.000000000000005329, 1.190312887963161259 ) ) ;
#35681=VERTEX_POINT ( 'NONE', #53375 ) ;
#35695=DIRECTION ( 'NONE',  ( 1.000000000000000000, 0.000000000000000000, 0.000000000000000000 ) ) ;
#35899=CARTESIAN_POINT ( 'NONE',  ( -2.244403820859648846, -9.000000000000005329, 0.2663676893020989755 ) ) ;
#35914=CARTESIAN_POINT ( 'NONE',  ( 7.749999999999993783, 9.491012693391979898E-16, 0.000000000000000000 ) ) ;
#35935=LINE ( 'NONE', #57381, #15815 ) ;
#35952=VECTOR ( 'NONE', #43691, 1000.000000000000000 ) ;
#36204=ORIENTED_EDGE ( 'NONE', *, *, #45647, .T. ) ;
#36210=VECTOR ( 'NONE', #18962, 1000.000000000000000 ) ;
#36268=DIRECTION ( 'NONE',  ( 1.000000000000000000, 0.000000000000000000, 0.000000000000000000 ) ) ;
#36420=CARTESIAN_POINT ( 'NONE',  ( 8.920833891111504599, -2.548662454712529613, 0.2685431138779699189 ) ) ;
#36468=FACE_OUTER_BOUND ( 'NONE', #63641, .T. ) ;
#36565=CARTESIAN_POINT ( 'NONE',  ( -5.603096392576912166, 8.295152368350910521, 0.9853608755428879817 ) ) ;
#36977=ORIENTED_EDGE ( 'NONE', *, *, #1776, .F. ) ;
#37156=CARTESIAN_POINT ( 'NONE',  ( 0.000000000000000000, 0.000000000000000000, 7.500000000000000000 ) ) ;
#37173=CARTESIAN_POINT ( 'NONE',  ( -7.794228634059950700, -4.500000000000003553, 0.000000000000000000 ) ) ;
#37233=B_SPLINE_CURVE_WITH_KNOTS ( 'NONE', 3,
 ( #41829, #24542, #14721, #52370, #36565, #9798 ),
 .UNSPECIFIED., .F., .F.,
 ( 4, 2, 4 ),
 ( 0.005386537104126978143, 0.008060814333094818568, 0.01073509156206266073 ),
 .UNSPECIFIED. ) ;
#37246=DIRECTION ( 'NONE',  ( -1.000000000000000000, -1.224646799147353454E-16, 0.000000000000000000 ) ) ;
#37431=CARTESIAN_POINT ( 'NONE',  ( -5.196152422706633800, -9.000000000000005329, 7.500000000000000000 ) ) ;
#37473=FACE_OUTER_BOUND ( 'NONE', #48703, .T. ) ;
#37556=PRODUCT_DEFINITION_CONTEXT ( 'detailed design', #32476, 'design' ) ;
#37630=AXIS2_PLACEMENT_3D ( 'NONE', #46661, #30064, #68080 ) ;
#37773=ORIENTED_EDGE ( 'NONE', *, *, #37976, .T. ) ;
#37799=AXIS2_PLACEMENT_3D ( 'NONE', #65092, #1736, #16947 ) ;
#37942=CARTESIAN_POINT ( 'NONE',  ( 0.000000000000000000, 9.000000000000007105, 0.000000000000000000 ) ) ;
#37976=EDGE_CURVE ( 'NONE', #16826, #8613, #67823, .T. ) ;
#37986=VERTEX_POINT ( 'NONE', #40913 ) ;
#38027=CARTESIAN_POINT ( 'NONE',  ( 0.000000000000000000, 0.000000000000000000, 7.500000000000000000 ) ) ;
#38074=ORIENTED_EDGE ( 'NONE', *, *, #31000, .F. ) ;
#38285=CARTESIAN_POINT ( 'NONE',  ( -4.377616827404060551, 9.000000000000010658, 1.000745235317163528 ) ) ;
#38298=EDGE_CURVE ( 'NONE', #69624, #66051, #6690, .T. ) ;
#38342=EDGE_LOOP ( 'NONE', ( #1202, #53053 ) ) ;
#38380=STYLED_ITEM ( 'NONE', ( #13790 ), #13706 ) ;
#38500=CARTESIAN_POINT ( 'NONE',  ( 7.794228634059952476, 4.500000000000003553, 0.000000000000000000 ) ) ;
#38539=ORIENTED_EDGE ( 'NONE', *, *, #47313, .F. ) ;
#38566=DIRECTION ( 'NONE',  ( -0.000000000000000000, -1.000000000000000000, -0.000000000000000000 ) ) ;
#38707=CARTESIAN_POINT ( 'NONE',  ( 1.800649583398763021, -9.000000000000007105, 0.1402270904467407264 ) ) ;
#38741=DIRECTION ( 'NONE',  ( 0.000000000000000000, 0.000000000000000000, 1.000000000000000000 ) ) ;
#38760=CARTESIAN_POINT ( 'NONE',  ( 10.39230484541327115, -4.119968255444916849E-15, 7.500000000000000000 ) ) ;
#38810=ORIENTED_EDGE ( 'NONE', *, *, #26292, .T. ) ;
#38843=DIRECTION ( 'NONE',  ( 0.000000000000000000, 0.000000000000000000, 1.000000000000000000 ) ) ;
#38887=DIRECTION ( 'NONE',  ( -1.000000000000000000, 0.000000000000000000, 0.000000000000000000 ) ) ;
#38979=CARTESIAN_POINT ( 'NONE',  ( -1.136396319700226032, 9.000000000000010658, 0.06877762208650195497 ) ) ;
#39069=DIRECTION ( 'NONE',  ( -0.000000000000000000, -0.000000000000000000, -1.000000000000000000 ) ) ;
#39263=ADVANCED_FACE ( 'NONE', ( #65811 ), #59835, .F. ) ;
#39341=( NAMED_UNIT ( * ) SI_UNIT ( $, .STERADIAN. ) SOLID_ANGLE_UNIT ( ) );
#39395=CARTESIAN_POINT ( 'NONE',  ( 0.000000000000000000, 9.000000000000007105, 0.000000000000000000 ) ) ;
#39414=DIRECTION ( 'NONE',  ( 1.000000000000000000, 0.000000000000000000, 0.000000000000000000 ) ) ;
#39420=FACE_BOUND ( 'NONE', #52847, .T. ) ;
#39429=EDGE_CURVE ( 'NONE', #69624, #65961, #56983, .T. ) ;
#39479=CIRCLE ( 'NONE', #9127, 9.000000000000007105 ) ;
#39507=CIRCLE ( 'NONE', #47406, 7.500000000000000000 ) ;
#39640=ORIENTED_EDGE ( 'NONE', *, *, #28226, .F. ) ;
#39845=B_SPLINE_CURVE_WITH_KNOTS ( 'NONE', 3,
 ( #63784, #58177, #51868, #36420, #3618, #62407, #41684, #31075 ),
 .UNSPECIFIED., .F., .F.,
 ( 4, 2, 2, 4 ),
 ( 2.544313220889483728E-07, 0.002693395767724532722, 0.004039966435925754565, 0.005386537104126976408 ),
 .UNSPECIFIED. ) ;
#39871=( NAMED_UNIT ( * ) SI_UNIT ( $, .STERADIAN. ) SOLID_ANGLE_UNIT ( ) );
#40162=FACE_OUTER_BOUND ( 'NONE', #18575, .T. ) ;
#40164=CARTESIAN_POINT ( 'NONE',  ( -0.2274700367024034831, -9.000000000000007105, -1.732394135371857768E-15 ) ) ;
#40384=VERTEX_POINT ( 'NONE', #8982 ) ;
#40444=CARTESIAN_POINT ( 'NONE',  ( -7.794228634059953364, 4.500000000000004441, 0.000000000000000000 ) ) ;
#40530=( NAMED_UNIT ( * ) SI_UNIT ( $, .STERADIAN. ) SOLID_ANGLE_UNIT ( ) );
#40693=DIRECTION ( 'NONE',  ( 0.000000000000000000, -0.000000000000000000, -1.000000000000000000 ) ) ;
#40902=SURFACE_STYLE_FILL_AREA ( #8527 ) ;
#40913=CARTESIAN_POINT ( 'NONE',  ( 0.000000000000000000, 9.000000000000007105, 0.000000000000000000 ) ) ;
#41023=AXIS2_PLACEMENT_3D ( 'NONE', #47072, #68499, #31883 ) ;
#41027=EDGE_LOOP ( 'NONE', ( #33951, #23777, #52267 ) ) ;
#41118=ORIENTED_EDGE ( 'NONE', *, *, #48798, .T. ) ;
#41559=STYLED_ITEM ( 'NONE', ( #6952 ), #51663 ) ;
#41684=CARTESIAN_POINT ( 'NONE',  ( 8.021777294149474713, -4.105874159530734424, 3.896351557369779711E-17 ) ) ;
#41686=CARTESIAN_POINT ( 'NONE',  ( 0.000000000000000000, 0.000000000000000000, 0.000000000000000000 ) ) ;
#41741=AXIS2_PLACEMENT_3D ( 'NONE', #24276, #45773, #18670 ) ;
#41745=PLANE ( 'NONE',  #50455 ) ;
#41793=ORIENTED_EDGE ( 'NONE', *, *, #62267, .F. ) ;
#41829=CARTESIAN_POINT ( 'NONE',  ( -7.794228634059953364, 4.500000000000004441, 0.000000000000000000 ) ) ;
#41831=ORIENTED_EDGE ( 'NONE', *, *, #8118, .F. ) ;
#41942=DIRECTION ( 'NONE',  ( -0.7071067811865500152, 0.000000000000000000, -0.7071067811865450192 ) ) ;
#41995=ADVANCED_FACE ( 'NONE', ( #17346 ), #50363, .T. ) ;
#42115=ORIENTED_EDGE ( 'NONE', *, *, #19765, .T. ) ;
#42153=CIRCLE ( 'NONE', #3857, 7.500000000000000000 ) ;
#42281=DIRECTION ( 'NONE',  ( 0.000000000000000000, 0.000000000000000000, 1.000000000000000000 ) ) ;
#42438=CIRCLE ( 'NONE', #46962, 9.000000000000007105 ) ;
#42486=DIRECTION ( 'NONE',  ( 1.000000000000000000, 0.000000000000000000, 0.000000000000000000 ) ) ;
#42582=ADVANCED_FACE ( 'NONE', ( #51567 ), #41745, .F. ) ;
#42840=AXIS2_PLACEMENT_3D ( 'NONE', #59977, #7217, #49786 ) ;
#42842=ORIENTED_EDGE ( 'NONE', *, *, #60494, .T. ) ;
#42875=FACE_OUTER_BOUND ( 'NONE', #21792, .T. ) ;
#42950=CARTESIAN_POINT ( 'NONE',  ( 5.196152422706636465, -9.000000000000005329, 1.392304845413258274 ) ) ;
#43016=EDGE_LOOP ( 'NONE', ( #58467, #24754, #9577 ) ) ;
#43456=CONICAL_SURFACE ( 'NONE', #52411, 9.000000000000007105, 0.7853981633974500554 ) ;
#43687=CARTESIAN_POINT ( 'NONE',  ( -5.196152422706634688, 9.000000000000008882, 7.500000000000000000 ) ) ;
#43691=DIRECTION ( 'NONE',  ( -0.000000000000000000, -0.000000000000000000, -1.000000000000000000 ) ) ;
#43763=CARTESIAN_POINT ( 'NONE',  ( 7.566679973970428463, 4.894125840469273570, -3.502763581212283073E-15 ) ) ;
#43828=MECHANICAL_DESIGN_GEOMETRIC_PRESENTATION_REPRESENTATION('',(#41559),#7822);
#43938=FACE_OUTER_BOUND ( 'NONE', #29627, .T. ) ;
#44244=VERTEX_POINT ( 'NONE', #66557 ) ;
#44283=AXIS2_PLACEMENT_3D ( 'NONE', #17894, #34063, #61464 ) ;
#44418=ORIENTED_EDGE ( 'NONE', *, *, #17203, .F. ) ;
#44506=ORIENTED_EDGE ( 'NONE', *, *, #11029, .F. ) ;
#44530=ORIENTED_EDGE ( 'NONE', *, *, #59944, .F. ) ;
#44667=DIRECTION ( 'NONE',  ( 1.000000000000000000, 0.000000000000000000, -0.000000000000000000 ) ) ;
#44956=CARTESIAN_POINT ( 'NONE',  ( -9.568252947146934417, 1.427299755870875320, 0.6386920474458039898 ) ) ;
#44984=DIRECTION ( 'NONE',  ( 0.000000000000000000, 0.000000000000000000, 1.000000000000000000 ) ) ;
#45287=CARTESIAN_POINT ( 'NONE',  ( 7.794228634059952476, 4.500000000000003553, 0.000000000000000000 ) ) ;
#45347=AXIS2_PLACEMENT_3D ( 'NONE', #2407, #29178, #61212 ) ;
#45383=AXIS2_PLACEMENT_3D ( 'NONE', #55863, #6613, #44667 ) ;
#45411=ADVANCED_FACE ( 'NONE', ( #66865 ), #3436, .T. ) ;
#45647=EDGE_CURVE ( 'NONE', #57711, #24348, #19185, .T. ) ;
#45713=CARTESIAN_POINT ( 'NONE',  ( -9.985360875542992787, -0.7048476316490953630, 0.9853608755428877597 ) ) ;
#45723=CARTESIAN_POINT ( 'NONE',  ( 0.000000000000000000, 0.000000000000000000, 0.000000000000000000 ) ) ;
#45773=DIRECTION ( 'NONE',  ( 0.000000000000000000, 0.000000000000000000, 1.000000000000000000 ) ) ;
#45790=CARTESIAN_POINT ( 'NONE',  ( -3.535366420403589061, -9.000000000000005329, 0.6617903051486780930 ) ) ;
#45797=ORIENTED_EDGE ( 'NONE', *, *, #27689, .F. ) ;
#45996=CARTESIAN_POINT ( 'NONE',  ( 5.196152422706629359, 9.000000000000008882, 1.392304845413260272 ) ) ;
#46180=( NAMED_UNIT ( * ) PLANE_ANGLE_UNIT ( ) SI_UNIT ( $, .RADIAN. ) );
#46234=ORIENTED_EDGE ( 'NONE', *, *, #3774, .T. ) ;
#46235=FACE_OUTER_BOUND ( 'NONE', #30060, .T. ) ;
#46388=EDGE_CURVE ( 'NONE', #7642, #40384, #65879, .T. ) ;
#46529=DIRECTION ( 'NONE',  ( 1.000000000000000000, 0.000000000000000000, 0.000000000000000000 ) ) ;
#46559=CARTESIAN_POINT ( 'NONE',  ( -5.196152422706634688, 9.000000000000008882, 7.500000000000000000 ) ) ;
#46616=DIRECTION ( 'NONE',  ( 0.000000000000000000, 0.000000000000000000, -1.000000000000000000 ) ) ;
#46661=CARTESIAN_POINT ( 'NONE',  ( 0.000000000000000000, 0.000000000000000000, 1.000000000000000000 ) ) ;
#46962=AXIS2_PLACEMENT_3D ( 'NONE', #21099, #42281, #15509 ) ;
#46982=CARTESIAN_POINT ( 'NONE',  ( -7.749999999999993783, 0.000000000000000000, 0.000000000000000000 ) ) ;
#47056=CARTESIAN_POINT ( 'NONE',  ( 5.196152422706636465, -9.000000000000005329, 7.500000000000000000 ) ) ;
#47072=CARTESIAN_POINT ( 'NONE',  ( 5.196152422706636465, -9.000000000000005329, 7.500000000000000000 ) ) ;
#47180=VERTEX_POINT ( 'NONE', #67571 ) ;
#47187=ORIENTED_EDGE ( 'NONE', *, *, #53824, .F. ) ;
#47313=EDGE_CURVE ( 'NONE', #35681, #44244, #63330, .T. ) ;
#47322=AXIS2_PLACEMENT_3D ( 'NONE', #58876, #18868, #35067 ) ;
#47325=DIRECTION ( 'NONE',  ( -1.000000000000000000, 0.000000000000000000, 0.000000000000000000 ) ) ;
#47406=AXIS2_PLACEMENT_3D ( 'NONE', #15312, #4707, #47325 ) ;
#47475=DIRECTION ( 'NONE',  ( 0.000000000000000000, 0.000000000000000000, 1.000000000000000000 ) ) ;
#47798=EDGE_CURVE ( 'NONE', #28130, #37986, #64126, .T. ) ;
#47828=ORIENTED_EDGE ( 'NONE', *, *, #38298, .F. ) ;
#48028=CARTESIAN_POINT ( 'NONE',  ( -7.335726704534229370, -5.294148637306920868, 0.03572125916566790127 ) ) ;
#48147=CARTESIAN_POINT ( 'NONE',  ( 0.000000000000000000, 0.000000000000000000, 7.500000000000000000 ) ) ;
#48477=EDGE_CURVE ( 'NONE', #47180, #35681, #29696, .T. ) ;
#48703=EDGE_LOOP ( 'NONE', ( #32769, #55359, #46234 ) ) ;
#48714=CARTESIAN_POINT ( 'NONE',  ( -6.887213563469348543, -6.070996185493598318, 0.1702817813269538461 ) ) ;
#48798=EDGE_CURVE ( 'NONE', #27464, #37986, #48868, .T. ) ;
#48803=( GEOMETRIC_REPRESENTATION_CONTEXT ( 3 ) GLOBAL_UNCERTAINTY_ASSIGNED_CONTEXT ( ( #52524 ) ) GLOBAL_UNIT_ASSIGNED_CONTEXT ( ( #29775, #51237, #52636 ) ) REPRESENTATION_CONTEXT ( 'NONE', 'WORKASPACE' ) );
#48856=AXIS2_PLACEMENT_3D ( 'NONE', #57736, #63691, #46529 ) ;
#48868=CIRCLE ( 'NONE', #61173, 9.000000000000007105 ) ;
#48948=FACE_OUTER_BOUND ( 'NONE', #14164, .T. ) ;
#49163=CARTESIAN_POINT ( 'NONE',  ( -5.196152422706634688, 9.000000000000008882, 1.392304845413263159 ) ) ;
#49573=DIRECTION ( 'NONE',  ( 0.000000000000000000, 0.000000000000000000, 1.000000000000000000 ) ) ;
#49786=DIRECTION ( 'NONE',  ( 1.000000000000000000, 0.000000000000000000, 0.000000000000000000 ) ) ;
#49850=CARTESIAN_POINT ( 'NONE',  ( -2.244403820859647070, 9.000000000000012434, 0.2663676893021043601 ) ) ;
#49905=CARTESIAN_POINT ( 'NONE',  ( 6.898093598910799429, -6.052151411320861207, 0.1381979515792686741 ) ) ;
#50034=CARTESIAN_POINT ( 'NONE',  ( 0.000000000000000000, 0.000000000000000000, 42.50000000000000000 ) ) ;
#50038=CARTESIAN_POINT ( 'NONE',  ( 0.000000000000000000, 0.000000000000000000, 0.7500000000000000000 ) ) ;
#50318=CARTESIAN_POINT ( 'NONE',  ( 5.196152422706629359, 9.000000000000008882, 7.500000000000000000 ) ) ;
#50346=CARTESIAN_POINT ( 'NONE',  ( 0.000000000000000000, 0.000000000000000000, 1.000000000000000000 ) ) ;
#50363=CYLINDRICAL_SURFACE ( 'NONE', #18944, 5.000000000000000000 ) ;
#50455=AXIS2_PLACEMENT_3D ( 'NONE', #69146, #52293, #40693 ) ;
#50664=FACE_OUTER_BOUND ( 'NONE', #29089, .T. ) ;
#50849=ADVANCED_FACE ( 'NONE', ( #67650 ), #19450, .F. ) ;
#50919=VERTEX_POINT ( 'NONE', #68703 ) ;
#50958=ORIENTED_EDGE ( 'NONE', *, *, #30772, .T. ) ;
#51068=( NAMED_UNIT ( * ) PLANE_ANGLE_UNIT ( ) SI_UNIT ( $, .RADIAN. ) );
#51103=DIRECTION ( 'NONE',  ( -0.000000000000000000, -0.000000000000000000, -1.000000000000000000 ) ) ;
#51165=AXIS2_PLACEMENT_3D ( 'NONE', #50346, #13382, #35561 ) ;
#51199=CARTESIAN_POINT ( 'NONE',  ( 0.000000000000000000, 0.000000000000000000, 0.2499999999999924227 ) ) ;
#51237=( NAMED_UNIT ( * ) PLANE_ANGLE_UNIT ( ) SI_UNIT ( $, .RADIAN. ) );
#51363=CARTESIAN_POINT ( 'NONE',  ( 5.196152422706629359, 9.000000000000008882, 7.500000000000000000 ) ) ;
#51410=APPLICATION_CONTEXT ( 'automotive_design' ) ;
#51567=FACE_OUTER_BOUND ( 'NONE', #59052, .T. ) ;
#51663=ADVANCED_FACE ( 'NONE', ( #43938 ), #31415, .F. ) ;
#51780=SURFACE_SIDE_STYLE ('',( #40902 ) ) ;
#51851=FACE_OUTER_BOUND ( 'NONE', #26428, .T. ) ;
#51868=CARTESIAN_POINT ( 'NONE',  ( 9.568252947146932641, -1.427299755870875986, 0.6386920474458026575 ) ) ;
#52148=CONICAL_SURFACE ( 'NONE', #44283, 9.000000000000007105, 0.7853981633974500554 ) ;
#52267=ORIENTED_EDGE ( 'NONE', *, *, #68375, .T. ) ;
#52280=FACE_BOUND ( 'NONE', #38342, .T. ) ;
#52293=DIRECTION ( 'NONE',  ( 0.000000000000000000, -1.000000000000000000, 0.000000000000000000 ) ) ;
#52370=CARTESIAN_POINT ( 'NONE',  ( -6.021969435454501252, 7.569642976165948056, 0.6362876910938565223 ) ) ;
#52411=AXIS2_PLACEMENT_3D ( 'NONE', #14011, #61821, #13653 ) ;
#52435=PRODUCT_DEFINITION ( 'UNKNOWN', '', #1144, #37556 ) ;
#52438=CARTESIAN_POINT ( 'NONE',  ( -5.196152422706633800, -9.000000000000005329, 7.500000000000000000 ) ) ;
#52460=DIRECTION ( 'NONE',  ( -0.000000000000000000, -0.000000000000000000, -1.000000000000000000 ) ) ;
#52524=UNCERTAINTY_MEASURE_WITH_UNIT (LENGTH_MEASURE( 1.000000000000000082E-05 ), #29775, 'distance_accuracy_value', 'NONE');
#52529=CARTESIAN_POINT ( 'NONE',  ( 7.249999999999999112, 9.031770143711729009E-16, 1.000000000000000000 ) ) ;
#52555=CARTESIAN_POINT ( 'NONE',  ( 0.000000000000000000, 0.000000000000000000, 0.000000000000000000 ) ) ;
#52559=CIRCLE ( 'NONE', #27785, 5.000000000000000000 ) ;
#52596=EDGE_LOOP ( 'NONE', ( #8985, #58182 ) ) ;
#52636=( NAMED_UNIT ( * ) SI_UNIT ( $, .STERADIAN. ) SOLID_ANGLE_UNIT ( ) );
#52668=FACE_OUTER_BOUND ( 'NONE', #204, .T. ) ;
#52718=CARTESIAN_POINT ( 'NONE',  ( 8.690363669209107300, 2.947848588679142789, 0.1381979515792646496 ) ) ;
#52847=EDGE_LOOP ( 'NONE', ( #42115, #1317 ) ) ;
#53001=ORIENTED_EDGE ( 'NONE', *, *, #47798, .F. ) ;
#53053=ORIENTED_EDGE ( 'NONE', *, *, #19136, .F. ) ;
#53375=CARTESIAN_POINT ( 'NONE',  ( -7.500000000000000000, 0.000000000000000000, 0.7500000000000000000 ) ) ;
#53454=ORIENTED_EDGE ( 'NONE', *, *, #68375, .F. ) ;
#53824=EDGE_CURVE ( 'NONE', #32384, #7642, #25541, .T. ) ;
#53950=ORIENTED_EDGE ( 'NONE', *, *, #48798, .F. ) ;
#54130=CARTESIAN_POINT ( 'NONE',  ( 0.000000000000000000, -9.000000000000007105, 0.000000000000000000 ) ) ;
#54384=EDGE_CURVE ( 'NONE', #12618, #2274, #23786, .T. ) ;
#54479=DIRECTION ( 'NONE',  ( 1.000000000000000000, 0.000000000000000000, 0.000000000000000000 ) ) ;
#54526=VECTOR ( 'NONE', #3955, 1000.000000000000227 ) ;
#54535=CARTESIAN_POINT ( 'NONE',  ( 5.000000000000000000, 6.123233995736766282E-16, 42.50000000000000000 ) ) ;
#54538=AXIS2_PLACEMENT_3D ( 'NONE', #45723, #12620, #66806 ) ;
#54589=DIRECTION ( 'NONE',  ( -1.000000000000000000, 0.000000000000000000, 0.000000000000000000 ) ) ;
#54948=CARTESIAN_POINT ( 'NONE',  ( 0.000000000000000000, 0.000000000000000000, 0.000000000000000000 ) ) ;
#55024=( GEOMETRIC_REPRESENTATION_CONTEXT ( 3 ) GLOBAL_UNCERTAINTY_ASSIGNED_CONTEXT ( ( #31859 ) ) GLOBAL_UNIT_ASSIGNED_CONTEXT ( ( #19404, #25034, #39871 ) ) REPRESENTATION_CONTEXT ( 'NONE', 'WORKASPACE' ) );
#55088=CARTESIAN_POINT ( 'NONE',  ( -0.2274700367024033443, 9.000000000000008882, 3.467894058216981173E-15 ) ) ;
#55130=EDGE_CURVE ( 'NONE', #40384, #33911, #13195, .T. ) ;
#55141=CARTESIAN_POINT ( 'NONE',  ( 7.342319042881621627, -5.282730372348553693, -4.573977915173220598E-17 ) ) ;
#55286=FILL_AREA_STYLE ('',( #13408 ) ) ;
#55306=FACE_OUTER_BOUND ( 'NONE', #20421, .T. ) ;
#55359=ORIENTED_EDGE ( 'NONE', *, *, #46388, .T. ) ;
#55486=( LENGTH_UNIT ( ) NAMED_UNIT ( * ) SI_UNIT ( .MILLI., .METRE. ) );
#55537=AXIS2_PLACEMENT_3D ( 'NONE', #65238, #38566, #28968 ) ;
#55548=LINE ( 'NONE', #6644, #5976 ) ;
#55814=CARTESIAN_POINT ( 'NONE',  ( -7.794228634059953364, 4.500000000000004441, 0.000000000000000000 ) ) ;
#55863=CARTESIAN_POINT ( 'NONE',  ( 0.000000000000000000, 0.000000000000000000, 42.50000000000000000 ) ) ;
#55876=CARTESIAN_POINT ( 'NONE',  ( -8.246138225238285102, -3.717269627651450303, -1.631385456411781861E-15 ) ) ;
#55928=VECTOR ( 'NONE', #31318, 1000.000000000000000 ) ;
#55988=ADVANCED_FACE ( 'NONE', ( #52280, #36468 ), #14994, .T. ) ;
#56080=ADVANCED_FACE ( 'NONE', ( #27903 ), #31911, .T. ) ;
#56120=CARTESIAN_POINT ( 'NONE',  ( -10.39230484541327293, 3.469446951953614189E-15, 7.500000000000000000 ) ) ;
#56217=CARTESIAN_POINT ( 'NONE',  ( 3.542013698345604755, 9.000000000000008882, 0.6642442188400928815 ) ) ;
#56288=CARTESIAN_POINT ( 'NONE',  ( 0.000000000000000000, 0.000000000000000000, 0.000000000000000000 ) ) ;
#56304=ORIENTED_EDGE ( 'NONE', *, *, #38298, .T. ) ;
#56335=VECTOR ( 'NONE', #9094, 1000.000000000000000 ) ;
#56360=CIRCLE ( 'NONE', #68797, 7.500000000000000000 ) ;
#56458=ORIENTED_EDGE ( 'NONE', *, *, #30772, .F. ) ;
#56612=VECTOR ( 'NONE', #52460, 1000.000000000000000 ) ;
#56675=CARTESIAN_POINT ( 'NONE',  ( 5.196152422706636465, -9.000000000000005329, 7.500000000000000000 ) ) ;
#56866=CARTESIAN_POINT ( 'NONE',  ( -8.701243704650558186, 2.929003814506410119, 0.1702817813269568992 ) ) ;
#56983=LINE ( 'NONE', #51363, #14146 ) ;
#57031=CARTESIAN_POINT ( 'NONE',  ( 7.500000000000000000, 9.184850993605147944E-16, 0.2499999999999924227 ) ) ;
#57267=EDGE_LOOP ( 'NONE', ( #4947, #53950, #12920 ) ) ;
#57381=CARTESIAN_POINT ( 'NONE',  ( -7.500000000000000000, 0.000000000000000000, 0.2499999999999924227 ) ) ;
#57461=DIRECTION ( 'NONE',  ( -1.000000000000000000, 0.000000000000000000, -0.000000000000000000 ) ) ;
#57711=VERTEX_POINT ( 'NONE', #52529 ) ;
#57736=CARTESIAN_POINT ( 'NONE',  ( 0.000000000000000000, 0.000000000000000000, 0.000000000000000000 ) ) ;
#57862=ORIENTED_EDGE ( 'NONE', *, *, #64729, .F. ) ;
#58083=ADVANCED_FACE ( 'NONE', ( #40162 ), #61556, .F. ) ;
#58177=CARTESIAN_POINT ( 'NONE',  ( 9.984889265949533410, -0.7056644834263142707, 0.9848892659495224189 ) ) ;
#58182=ORIENTED_EDGE ( 'NONE', *, *, #17131, .T. ) ;
#58347=ORIENTED_EDGE ( 'NONE', *, *, #66978, .F. ) ;
#58404=DIRECTION ( 'NONE',  ( 0.000000000000000000, 0.000000000000000000, 1.000000000000000000 ) ) ;
#58452=EDGE_CURVE ( 'NONE', #29727, #60346, #8693, .T. ) ;
#58458=AXIS2_PLACEMENT_3D ( 'NONE', #22521, #38741, #22171 ) ;
#58467=ORIENTED_EDGE ( 'NONE', *, *, #59974, .T. ) ;
#58566=ORIENTED_EDGE ( 'NONE', *, *, #19941, .T. ) ;
#58629=PLANE ( 'NONE',  #41023 ) ;
#58823=VERTEX_POINT ( 'NONE', #56120 ) ;
#58851=CARTESIAN_POINT ( 'NONE',  ( -5.196152422706633800, -9.000000000000005329, 7.500000000000000000 ) ) ;
#58872=AXIS2_PLACEMENT_3D ( 'NONE', #184, #4116, #37246 ) ;
#58876=CARTESIAN_POINT ( 'NONE',  ( 0.000000000000000000, 0.000000000000000000, 0.000000000000000000 ) ) ;
#59052=EDGE_LOOP ( 'NONE', ( #53001, #61170, #24043, #56304, #39640 ) ) ;
#59323=DIRECTION ( 'NONE',  ( 0.000000000000000000, 0.000000000000000000, 1.000000000000000000 ) ) ;
#59354=EDGE_CURVE ( 'NONE', #27464, #28130, #37233, .T. ) ;
#59408=CARTESIAN_POINT ( 'NONE',  ( -5.196152422706634688, 9.000000000000008882, 1.392304845413263159 ) ) ;
#59416=ORIENTED_EDGE ( 'NONE', *, *, #66978, .T. ) ;
#59563=EDGE_LOOP ( 'NONE', ( #26694, #8008, #44418, #33090 ) ) ;
#59581=CARTESIAN_POINT ( 'NONE',  ( -7.249999999999999112, 0.000000000000000000, 1.000000000000000000 ) ) ;
#59592=DIRECTION ( 'NONE',  ( 0.000000000000000000, 0.000000000000000000, 1.000000000000000000 ) ) ;
#59654=DIRECTION ( 'NONE',  ( -1.000000000000000000, 0.000000000000000000, 0.000000000000000000 ) ) ;
#59657=AXIS2_PLACEMENT_3D ( 'NONE', #34897, #34544, #67254 ) ;
#59835=PLANE ( 'NONE',  #37799 ) ;
#59944=EDGE_CURVE ( 'NONE', #27464, #16826, #39479, .T. ) ;
#59954=CIRCLE ( 'NONE', #68970, 7.249999999999999112 ) ;
#59971=ADVANCED_FACE ( 'NONE', ( #37473 ), #7954, .T. ) ;
#59972=ORIENTED_EDGE ( 'NONE', *, *, #17203, .T. ) ;
#59974=EDGE_CURVE ( 'NONE', #66051, #2274, #8665, .T. ) ;
#59977=CARTESIAN_POINT ( 'NONE',  ( 0.000000000000000000, 0.000000000000000000, 0.000000000000000000 ) ) ;
#60089=CARTESIAN_POINT ( 'NONE',  ( 5.196152422706636465, -9.000000000000005329, 1.392304845413258274 ) ) ;
#60140=ADVANCED_FACE ( 'NONE', ( #55306 ), #61924, .F. ) ;
#60346=VERTEX_POINT ( 'NONE', #54535 ) ;
#60406=EDGE_CURVE ( 'NONE', #65961, #58823, #22189, .T. ) ;
#60420=CARTESIAN_POINT ( 'NONE',  ( 5.603096392576913054, -8.295152368350905192, 0.9853608755428857613 ) ) ;
#60453=CARTESIAN_POINT ( 'NONE',  ( 1.800649583398759468, 9.000000000000008882, 0.1402270904467449175 ) ) ;
#60494=EDGE_CURVE ( 'NONE', #60346, #4855, #67173, .T. ) ;
#60545=PRESENTATION_STYLE_ASSIGNMENT (( #17687 ) ) ;
#60565=CARTESIAN_POINT ( 'NONE',  ( 6.667623377008398577, 6.451337545287478825, 0.2685431138779675320 ) ) ;
#60936=CIRCLE ( 'NONE', #9306, 5.000000000000000000 ) ;
#61109=CIRCLE ( 'NONE', #58872, 0.2500000000000002220 ) ;
#61170=ORIENTED_EDGE ( 'NONE', *, *, #21432, .F. ) ;
#61173=AXIS2_PLACEMENT_3D ( 'NONE', #30220, #3464, #14078 ) ;
#61212=DIRECTION ( 'NONE',  ( -1.000000000000000000, 0.000000000000000000, 0.000000000000000000 ) ) ;
#61443=ADVANCED_FACE ( 'NONE', ( #50664 ), #9378, .F. ) ;
#61464=DIRECTION ( 'NONE',  ( -1.000000000000000000, 0.000000000000000000, 0.000000000000000000 ) ) ;
#61556=CYLINDRICAL_SURFACE ( 'NONE', #51165, 7.500000000000000000 ) ;
#61821=DIRECTION ( 'NONE',  ( 0.000000000000000000, 0.000000000000000000, 1.000000000000000000 ) ) ;
#61924=CONICAL_SURFACE ( 'NONE', #59657, 7.500000000000000000, 0.7853981633974518317 ) ;
#62125=CARTESIAN_POINT ( 'NONE',  ( 7.794228634059951588, -4.500000000000003553, 0.000000000000000000 ) ) ;
#62192=ADVANCED_FACE ( 'NONE', ( #30758 ), #3293, .F. ) ;
#62267=EDGE_CURVE ( 'NONE', #16387, #44244, #42153, .T. ) ;
#62278=CARTESIAN_POINT ( 'NONE',  ( -3.109213548236405611, -9.000000000000007105, 0.5129086262188669032 ) ) ;
#62407=CARTESIAN_POINT ( 'NONE',  ( 8.252730563585677359, -3.705851362693088458, 0.03572125916567005927 ) ) ;
#62599=LINE ( 'NONE', #52438, #24000 ) ;
#62610=CARTESIAN_POINT ( 'NONE',  ( 0.000000000000000000, -9.000000000000007105, 0.000000000000000000 ) ) ;
#62658=ADVANCED_FACE ( 'NONE', ( #42875 ), #10129, .T. ) ;
#62717=EDGE_CURVE ( 'NONE', #57711, #47180, #61109, .T. ) ;
#63059=DIRECTION ( 'NONE',  ( 0.000000000000000000, 1.000000000000000000, 0.000000000000000000 ) ) ;
#63209=DIRECTION ( 'NONE',  ( 0.000000000000000000, 0.000000000000000000, -1.000000000000000000 ) ) ;
#63330=LINE ( 'NONE', #26379, #56612 ) ;
#63482=DIRECTION ( 'NONE',  ( 0.000000000000000000, 0.000000000000000000, -1.000000000000000000 ) ) ;
#63641=EDGE_LOOP ( 'NONE', ( #24016, #22914, #50958, #22944, #4690, #2163 ) ) ;
#63644=ORIENTED_EDGE ( 'NONE', *, *, #5650, .F. ) ;
#63691=DIRECTION ( 'NONE',  ( 0.000000000000000000, 0.000000000000000000, 1.000000000000000000 ) ) ;
#63748=CARTESIAN_POINT ( 'NONE',  ( -5.196152422706634688, 9.000000000000008882, 7.500000000000000000 ) ) ;
#63784=CARTESIAN_POINT ( 'NONE',  ( 10.39230484541327115, -3.482307324624967703E-15, 1.392304845413258718 ) ) ;
#63898=ORIENTED_EDGE ( 'NONE', *, *, #59944, .T. ) ;
#63929=CARTESIAN_POINT ( 'NONE',  ( 0.000000000000000000, 0.000000000000000000, 1.000000000000000000 ) ) ;
#64053=EDGE_LOOP ( 'NONE', ( #58566, #10524, #65807 ) ) ;
#64089=ORIENTED_EDGE ( 'NONE', *, *, #27142, .T. ) ;
#64095=DIRECTION ( 'NONE',  ( 0.000000000000000000, -0.000000000000000000, 1.000000000000000000 ) ) ;
#64126=B_SPLINE_CURVE_WITH_KNOTS ( 'NONE', 3,
 ( #49163, #28344, #38285, #861, #17506, #49850, #1588, #38979, #5864, #23113, #55088, #37942 ),
 .UNSPECIFIED., .F., .F.,
 ( 4, 2, 2, 2, 2, 4 ),
 ( 0.007986462481733982294, 0.009333070490708115369, 0.01067967849968225018, 0.01202628650865638499, 0.01269959051314345153, 0.01337289451763051980 ),
 .UNSPECIFIED. ) ;
#64289=CARTESIAN_POINT ( 'NONE',  ( 7.794228634059952476, 4.500000000000003553, 0.000000000000000000 ) ) ;
#64459=ORIENTED_EDGE ( 'NONE', *, *, #27225, .F. ) ;
#64643=DIRECTION ( 'NONE',  ( 0.000000000000000000, 0.000000000000000000, -1.000000000000000000 ) ) ;
#64729=EDGE_CURVE ( 'NONE', #8613, #27375, #9896, .T. ) ;
#64777=ADVANCED_FACE ( 'NONE', ( #8398 ), #43456, .T. ) ;
#64784=PRODUCT ( '10. Bolt M10x25', '10. Bolt M10x25', '', ( #34630 ) ) ;
#64828=CARTESIAN_POINT ( 'NONE',  ( 6.887213563469345878, 6.070996185493600095, 0.1702817813269535685 ) ) ;
#64925=ORIENTED_EDGE ( 'NONE', *, *, #11757, .T. ) ;
#64982=CARTESIAN_POINT ( 'NONE',  ( -10.39230484541327293, 3.469446951953614189E-15, 7.500000000000000000 ) ) ;
#65092=CARTESIAN_POINT ( 'NONE',  ( 10.39230484541327115, -4.119968255444916849E-15, 7.500000000000000000 ) ) ;
#65119=EDGE_LOOP ( 'NONE', ( #63898, #34352, #9294 ) ) ;
#65238=CARTESIAN_POINT ( 'NONE',  ( -7.249999999999999112, 0.000000000000000000, 0.7500000000000000000 ) ) ;
#65477=TOROIDAL_SURFACE ( 'NONE', #26147, 7.249999999999999112, 0.2500000000000000000 ) ;
#65492=DIRECTION ( 'NONE',  ( -0.000000000000000000, -0.000000000000000000, -1.000000000000000000 ) ) ;
#65528=EDGE_CURVE ( 'NONE', #3314, #4855, #52559, .T. ) ;
#65572=CARTESIAN_POINT ( 'NONE',  ( 0.000000000000000000, 0.000000000000000000, 0.000000000000000000 ) ) ;
#65804=LINE ( 'NONE', #17303, #26190 ) ;
#65807=ORIENTED_EDGE ( 'NONE', *, *, #54384, .T. ) ;
#65811=FACE_OUTER_BOUND ( 'NONE', #33780, .T. ) ;
#65869=( LENGTH_UNIT ( ) NAMED_UNIT ( * ) SI_UNIT ( .MILLI., .METRE. ) );
#65879=B_SPLINE_CURVE_WITH_KNOTS ( 'NONE', 3,
 ( #42950, #22835, #16884, #27032, #10890, #38707, #32332, #54130 ),
 .UNSPECIFIED., .F., .F.,
 ( 4, 2, 2, 4 ),
 ( 0.005429405001700385487, 0.006777257746060603126, 0.008125110490420819898, 0.01082081597914125344 ),
 .UNSPECIFIED. ) ;
#65961=VERTEX_POINT ( 'NONE', #27313 ) ;
#65970=AXIS2_PLACEMENT_3D ( 'NONE', #18598, #49573, #54479 ) ;
#66043=CARTESIAN_POINT ( 'NONE',  ( 0.000000000000000000, 0.000000000000000000, 0.000000000000000000 ) ) ;
#66051=VERTEX_POINT ( 'NONE', #35407 ) ;
#66092=DIRECTION ( 'NONE',  ( 0.000000000000000000, 0.000000000000000000, 1.000000000000000000 ) ) ;
#66353=ORIENTED_EDGE ( 'NONE', *, *, #59354, .F. ) ;
#66362=CARTESIAN_POINT ( 'NONE',  ( -8.920833891111504599, 2.548662454712528724, 0.2685431138779709737 ) ) ;
#66372=AXIS2_PLACEMENT_3D ( 'NONE', #34092, #66092, #17918 ) ;
#66401=CARTESIAN_POINT ( 'NONE',  ( 7.794228634059951588, -4.500000000000003553, 0.000000000000000000 ) ) ;
#66437=CARTESIAN_POINT ( 'NONE',  ( 4.383403428314264438, 9.000000000000012434, 1.003298500868274434 ) ) ;
#66557=CARTESIAN_POINT ( 'NONE',  ( -7.500000000000000000, 0.000000000000000000, 0.2499999999999924227 ) ) ;
#66700=ORIENTED_EDGE ( 'NONE', *, *, #58452, .F. ) ;
#66806=DIRECTION ( 'NONE',  ( -1.000000000000000000, 0.000000000000000000, 0.000000000000000000 ) ) ;
#66865=FACE_OUTER_BOUND ( 'NONE', #41027, .T. ) ;
#66871=DIRECTION ( 'NONE',  ( 0.000000000000000000, 0.000000000000000000, 1.000000000000000000 ) ) ;
#66882=CARTESIAN_POINT ( 'NONE',  ( -0.4573008633723373850, -9.000000000000007105, 0.008766315107676130383 ) ) ;
#66903=SURFACE_SIDE_STYLE ('',( #23286 ) ) ;
#66978=EDGE_CURVE ( 'NONE', #16387, #28040, #556, .T. ) ;
#67173=LINE ( 'NONE', #23233, #36210 ) ;
#67254=DIRECTION ( 'NONE',  ( -1.000000000000000000, 0.000000000000000000, 0.000000000000000000 ) ) ;
#67419=CARTESIAN_POINT ( 'NONE',  ( 5.603568002170367102, 8.294335516573697831, 0.9848892659495218638 ) ) ;
#67544=AXIS2_PLACEMENT_3D ( 'NONE', #34301, #23737, #35695 ) ;
#67559=CARTESIAN_POINT ( 'NONE',  ( -1.136396319700227586, -9.000000000000005329, 0.06877762208649663977 ) ) ;
#67571=CARTESIAN_POINT ( 'NONE',  ( 7.500000000000000000, 9.184850993605147944E-16, 0.7500000000000000000 ) ) ;
#67650=FACE_OUTER_BOUND ( 'NONE', #1029, .T. ) ;
#67654=CARTESIAN_POINT ( 'NONE',  ( -10.39230484541327293, 3.469446951953614189E-15, 7.500000000000000000 ) ) ;
#67759=FILL_AREA_STYLE_COLOUR ( '', #26254 ) ;
#67823=CIRCLE ( 'NONE', #31901, 9.000000000000007105 ) ;
#67902=DIRECTION ( 'NONE',  ( -1.000000000000000000, 0.000000000000000000, 0.000000000000000000 ) ) ;
#67996=ORIENTED_EDGE ( 'NONE', *, *, #12053, .F. ) ;
#68080=DIRECTION ( 'NONE',  ( -1.000000000000000000, 0.000000000000000000, 0.000000000000000000 ) ) ;
#68269=ORIENTED_EDGE ( 'NONE', *, *, #54384, .F. ) ;
#68353=AXIS2_PLACEMENT_3D ( 'NONE', #37431, #63059, #64095 ) ;
#68375=EDGE_CURVE ( 'NONE', #8613, #40384, #31334, .T. ) ;
#68494=COLOUR_RGB ( '', 0.09019608, 0.27058824, 0.51372549) ;
#68499=DIRECTION ( 'NONE',  ( -0.8660254037844385966, 0.5000000000000002220, 0.000000000000000000 ) ) ;
#68668=COLOUR_RGB ( '', 0.09019608, 0.27058824, 0.51372549) ;
#68685=PRODUCT_DEFINITION_SHAPE ( 'NONE', 'NONE',  #52435 ) ;
#68703=CARTESIAN_POINT ( 'NONE',  ( 10.39230484541327115, -3.482307324624967703E-15, 1.392304845413258718 ) ) ;
#68797=AXIS2_PLACEMENT_3D ( 'NONE', #19934, #63209, #42486 ) ;
#68853=STYLED_ITEM ( 'NONE', ( #60545 ), #28952 ) ;
#68950=AXIS2_PLACEMENT_3D ( 'NONE', #66043, #44984, #17872 ) ;
#68970=AXIS2_PLACEMENT_3D ( 'NONE', #63929, #64643, #26964 ) ;
#69146=CARTESIAN_POINT ( 'NONE',  ( 5.196152422706629359, 9.000000000000008882, 7.500000000000000000 ) ) ;
#69183=VECTOR ( 'NONE', #1765, 1000.000000000000227 ) ;
#69508=ORIENTED_EDGE ( 'NONE', *, *, #48477, .T. ) ;
#69521=ORIENTED_EDGE ( 'NONE', *, *, #22287, .T. ) ;
#69578=DIRECTION ( 'NONE',  ( 0.8660254037844385966, 0.5000000000000002220, -0.000000000000000000 ) ) ;
#69587=ORIENTED_EDGE ( 'NONE', *, *, #47313, .T. ) ;
#69624=VERTEX_POINT ( 'NONE', #3343 ) ;
ENDSEC;
END-ISO-10303-21;
